ISO-10303-21;
HEADER;
FILE_DESCRIPTION (('STEP AP214'),
    '1' );
FILE_NAME ('basic internal retaining ring_ai_B27.1 - NA2-131.step',
    '2026-10-08T13:22:57',
    ( '' ),
    ( '' ),
    'SwSTEP 2.0',
    'SolidWorks 2026',
    '' );
FILE_SCHEMA (( 'AUTOMOTIVE_DESIGN' ));
ENDSEC;

DATA;
#4=CARTESIAN_POINT ( 'NONE',  ( 0.000000000000000000, 0.000000000000000000, -1.270000000000007123 ) ) ;
#8=AXIS2_PLACEMENT_3D ( 'NONE', #6315, #4531, #6166 ) ;
#10=LINE ( 'NONE', #4146, #4138 ) ;
#19=AXIS2_PLACEMENT_3D ( 'NONE', #2999, #9984, #6972 ) ;
#22=CARTESIAN_POINT ( 'NONE',  ( 15.44569104238500046, -1.018491042385001544, -1.270000000000007123 ) ) ;
#45=DIRECTION ( 'NONE',  ( 1.000000000000000000, 0.000000000000000000, 0.000000000000000000 ) ) ;
#51=CARTESIAN_POINT ( 'NONE',  ( 17.72919999999999874, 0.000000000000000000, -1.270000000000007123 ) ) ;
#54=EDGE_LOOP ( 'NONE', ( #8916, #8035, #5862, #4936 ) ) ;
#92=ORIENTED_EDGE ( 'NONE', *, *, #7588, .T. ) ;
#94=VERTEX_POINT ( 'NONE', #2924 ) ;
#100=EDGE_CURVE ( 'NONE', #8895, #4771, #529, .T. ) ;
#119=CYLINDRICAL_SURFACE ( 'NONE', #383, 0.9906000000000003691 ) ;
#127=EDGE_LOOP ( 'NONE', ( #6964, #4432, #9166, #5764, #3012, #4282, #881, #9298, #4822, #5247, #5054, #1752, #8600 ) ) ;
#145=EDGE_LOOP ( 'NONE', ( #8443, #9716, #3991, #7695 ) ) ;
#162=DIRECTION ( 'NONE',  ( 1.000000000000000000, 0.000000000000000000, 0.000000000000000000 ) ) ;
#188=CARTESIAN_POINT ( 'NONE',  ( 5.986002070941135678, -13.58603705635637304, -1.270000000000007123 ) ) ;
#218=DIRECTION ( 'NONE',  ( 0.000000000000000000, -6.338944243255235518E-49, 1.000000000000000000 ) ) ;
#245=CARTESIAN_POINT ( 'NONE',  ( 0.000000000000000000, 0.000000000000000000, 0.000000000000000000 ) ) ;
#248=DIRECTION ( 'NONE',  ( 0.000000000000000000, 6.338944243255235518E-49, -1.000000000000000000 ) ) ;
#253=CARTESIAN_POINT ( 'NONE',  ( -17.72919999999999874, 2.171200803144325526E-15, 1.376312083204286382E-63 ) ) ;
#273=VERTEX_POINT ( 'NONE', #6004 ) ;
#276=CARTESIAN_POINT ( 'NONE',  ( 0.000000000000000000, -1.018491042385001544, 0.000000000000000000 ) ) ;
#283=AXIS2_PLACEMENT_3D ( 'NONE', #9014, #7552, #10191 ) ;
#285=VERTEX_POINT ( 'NONE', #7734 ) ;
#318=LINE ( 'NONE', #5785, #2654 ) ;
#331=CYLINDRICAL_SURFACE ( 'NONE', #1163, 15.44569104238500046 ) ;
#341=DIRECTION ( 'NONE',  ( -0.9575619921529162637, -0.2882273949230683141, -3.311798021194104978E-34 ) ) ;
#356=ORIENTED_EDGE ( 'NONE', *, *, #8845, .T. ) ;
#374=SURFACE_SIDE_STYLE ('',( #9112 ) ) ;
#383=AXIS2_PLACEMENT_3D ( 'NONE', #7978, #9740, #5647 ) ;
#390=FACE_OUTER_BOUND ( 'NONE', #54, .T. ) ;
#407=ORIENTED_EDGE ( 'NONE', *, *, #4270, .T. ) ;
#417=EDGE_CURVE ( 'NONE', #5816, #3063, #2247, .T. ) ;
#428=CARTESIAN_POINT ( 'NONE',  ( 15.44569104238500046, -1.018491042385001544, -1.270000000000007123 ) ) ;
#429=EDGE_CURVE ( 'NONE', #7540, #5816, #4809, .T. ) ;
#455=ORIENTED_EDGE ( 'NONE', *, *, #7282, .T. ) ;
#487=DIRECTION ( 'NONE',  ( 0.000000000000000000, -6.338944243255235518E-49, 1.000000000000000000 ) ) ;
#489=DIRECTION ( 'NONE',  ( 1.000000000000000000, 0.000000000000000000, 0.000000000000000000 ) ) ;
#505=ORIENTED_EDGE ( 'NONE', *, *, #1535, .T. ) ;
#529=CIRCLE ( 'NONE', #2831, 17.72919999999999874 ) ;
#531=AXIS2_PLACEMENT_3D ( 'NONE', #7567, #3693, #489 ) ;
#532=CARTESIAN_POINT ( 'NONE',  ( 4.995402070941135086, -13.58603705635637304, -1.270000000000007123 ) ) ;
#559=ORIENTED_EDGE ( 'NONE', *, *, #2679, .F. ) ;
#572=DIRECTION ( 'NONE',  ( 0.000000000000000000, -6.338944243255235518E-49, 1.000000000000000000 ) ) ;
#586=DIRECTION ( 'NONE',  ( 0.000000000000000000, -6.338944243255235518E-49, 1.000000000000000000 ) ) ;
#598=CARTESIAN_POINT ( 'NONE',  ( -4.995402070941133310, -13.58603705635637304, -1.270000000000007123 ) ) ;
#623=AXIS2_PLACEMENT_3D ( 'NONE', #823, #981, #8843 ) ;
#677=CARTESIAN_POINT ( 'NONE',  ( -5.986002070941133901, -13.58603705635637304, -1.270000000000007123 ) ) ;
#683=DIRECTION ( 'NONE',  ( 0.000000000000000000, -6.338944243255235518E-49, 1.000000000000000000 ) ) ;
#688=VECTOR ( 'NONE', #1379, 1000.000000000000000 ) ;
#702=ORIENTED_EDGE ( 'NONE', *, *, #2541, .T. ) ;
#710=CARTESIAN_POINT ( 'NONE',  ( 11.48991645990273724, -11.34085470199652512, -1.270000000000007123 ) ) ;
#728=VERTEX_POINT ( 'NONE', #4678 ) ;
#738=ORIENTED_EDGE ( 'NONE', *, *, #3509, .T. ) ;
#750=EDGE_LOOP ( 'NONE', ( #8233, #3945, #2776, #7235 ) ) ;
#775=CYLINDRICAL_SURFACE ( 'NONE', #4084, 3.632200000000000539 ) ;
#800=CARTESIAN_POINT ( 'NONE',  ( -5.110041130070070992, -16.97680807127747826, -1.270000000000007123 ) ) ;
#805=CARTESIAN_POINT ( 'NONE',  ( -5.986002070941136566, -13.58603705635637482, 0.000000000000000000 ) ) ;
#823=CARTESIAN_POINT ( 'NONE',  ( 0.000000000000000000, 0.000000000000000000, 0.000000000000000000 ) ) ;
#841=AXIS2_PLACEMENT_3D ( 'NONE', #6825, #4314, #6714 ) ;
#843=CIRCLE ( 'NONE', #1171, 15.44569104238500046 ) ;
#850=DIRECTION ( 'NONE',  ( 1.000000000000000000, 0.000000000000000000, 0.000000000000000000 ) ) ;
#865=DIRECTION ( 'NONE',  ( 1.000000000000000000, 0.000000000000000000, 0.000000000000000000 ) ) ;
#867=ADVANCED_FACE ( 'NONE', ( #9741 ), #4252, .F. ) ;
#881=ORIENTED_EDGE ( 'NONE', *, *, #2812, .F. ) ;
#883=DIRECTION ( 'NONE',  ( 1.000000000000000000, 0.000000000000000000, 0.000000000000000000 ) ) ;
#885=AXIS2_PLACEMENT_3D ( 'NONE', #5887, #6702, #8433 ) ;
#889=CARTESIAN_POINT ( 'NONE',  ( -8.787954181158717404, -8.913453481710840620, 0.000000000000000000 ) ) ;
#903=ADVANCED_FACE ( 'NONE', ( #1823 ), #1060, .F. ) ;
#926=CYLINDRICAL_SURFACE ( 'NONE', #6587, 17.72919999999999874 ) ;
#930=ORIENTED_EDGE ( 'NONE', *, *, #4549, .T. ) ;
#954=DIRECTION ( 'NONE',  ( 0.000000000000000000, 6.338944243255235518E-49, -1.000000000000000000 ) ) ;
#981=DIRECTION ( 'NONE',  ( 0.000000000000000000, -6.338944243255235518E-49, 1.000000000000000000 ) ) ;
#1000=CARTESIAN_POINT ( 'NONE',  ( -5.986002070941136566, -13.58603705635637482, -1.270000000000007123 ) ) ;
#1047=SHAPE_REPRESENTATION ( 'basic internal retaining ring_ai_B27.1 - NA2-131', ( #3995 ), #7950 ) ;
#1055=EDGE_CURVE ( 'NONE', #4850, #4954, #4759, .T. ) ;
#1060=CYLINDRICAL_SURFACE ( 'NONE', #7772, 15.44569104238500046 ) ;
#1061=EDGE_CURVE ( 'NONE', #4771, #1717, #2795, .T. ) ;
#1067=ORIENTED_EDGE ( 'NONE', *, *, #429, .T. ) ;
#1159=ORIENTED_EDGE ( 'NONE', *, *, #2378, .F. ) ;
#1162=LINE ( 'NONE', #7464, #7266 ) ;
#1163=AXIS2_PLACEMENT_3D ( 'NONE', #9798, #7508, #3574 ) ;
#1171=AXIS2_PLACEMENT_3D ( 'NONE', #4561, #7661, #9318 ) ;
#1177=CARTESIAN_POINT ( 'NONE',  ( -5.110041130070070992, -16.97680807127747826, 0.000000000000000000 ) ) ;
#1206=DIRECTION ( 'NONE',  ( 1.000000000000000000, 0.000000000000000000, 0.000000000000000000 ) ) ;
#1215=PRODUCT_DEFINITION_SHAPE ( 'NONE', 'NONE',  #7252 ) ;
#1273=ORIENTED_EDGE ( 'NONE', *, *, #3129, .T. ) ;
#1309=VERTEX_POINT ( 'NONE', #8613 ) ;
#1331=CIRCLE ( 'NONE', #9599, 0.9906000000000003691 ) ;
#1333=AXIS2_PLACEMENT_3D ( 'NONE', #9076, #9227, #8341 ) ;
#1359=CIRCLE ( 'NONE', #1333, 3.632199999999998763 ) ;
#1379=DIRECTION ( 'NONE',  ( 0.000000000000000000, -6.338944243255235518E-49, 1.000000000000000000 ) ) ;
#1386=ORIENTED_EDGE ( 'NONE', *, *, #2260, .F. ) ;
#1397=EDGE_LOOP ( 'NONE', ( #7018, #1159 ) ) ;
#1435=CARTESIAN_POINT ( 'NONE',  ( -17.72919999999999874, 2.171200803144325526E-15, -1.270000000000007123 ) ) ;
#1449=VECTOR ( 'NONE', #9977, 999.9999999999998863 ) ;
#1454=DIRECTION ( 'NONE',  ( 0.000000000000000000, -6.338944243255235518E-49, 1.000000000000000000 ) ) ;
#1464=CARTESIAN_POINT ( 'NONE',  ( -4.169902070941136074, -13.58603705635637482, -1.270000000000007123 ) ) ;
#1473=EDGE_CURVE ( 'NONE', #6295, #7986, #3303, .T. ) ;
#1475=PLANE ( 'NONE',  #8773 ) ;
#1495=ADVANCED_FACE ( 'NONE', ( #5050 ), #926, .T. ) ;
#1499=VERTEX_POINT ( 'NONE', #2520 ) ;
#1507=AXIS2_PLACEMENT_3D ( 'NONE', #10054, #8611, #3805 ) ;
#1527=CARTESIAN_POINT ( 'NONE',  ( -5.110041130070070992, -16.97680807127747826, -1.270000000000007123 ) ) ;
#1535=EDGE_CURVE ( 'NONE', #5109, #9801, #2466, .T. ) ;
#1555=ORIENTED_EDGE ( 'NONE', *, *, #7726, .T. ) ;
#1560=DIRECTION ( 'NONE',  ( 1.000000000000000000, 0.000000000000000000, 0.000000000000000000 ) ) ;
#1579=CARTESIAN_POINT ( 'NONE',  ( 0.000000000000000000, 0.000000000000000000, 0.000000000000000000 ) ) ;
#1591=( NAMED_UNIT ( * ) PLANE_ANGLE_UNIT ( ) SI_UNIT ( $, .RADIAN. ) );
#1670=AXIS2_PLACEMENT_3D ( 'NONE', #4015, #7834, #865 ) ;
#1690=STYLED_ITEM ( 'NONE', ( #7394 ), #2769 ) ;
#1708=DIRECTION ( 'NONE',  ( 0.000000000000000000, 6.338944243255235518E-49, -1.000000000000000000 ) ) ;
#1717=VERTEX_POINT ( 'NONE', #1177 ) ;
#1752=ORIENTED_EDGE ( 'NONE', *, *, #6023, .F. ) ;
#1767=AXIS2_PLACEMENT_3D ( 'NONE', #5692, #8860, #1773 ) ;
#1773=DIRECTION ( 'NONE',  ( 1.000000000000000000, 0.000000000000000000, 0.000000000000000000 ) ) ;
#1776=DIRECTION ( 'NONE',  ( 0.000000000000000000, -6.338944243255235518E-49, 1.000000000000000000 ) ) ;
#1786=DIRECTION ( 'NONE',  ( 1.000000000000000000, 0.000000000000000000, 0.000000000000000000 ) ) ;
#1816=CARTESIAN_POINT ( 'NONE',  ( -5.986002070941136566, -13.58603705635637482, 0.000000000000000000 ) ) ;
#1818=EDGE_CURVE ( 'NONE', #7986, #4850, #9758, .T. ) ;
#1823=FACE_OUTER_BOUND ( 'NONE', #750, .T. ) ;
#1836=DIRECTION ( 'NONE',  ( 0.000000000000000000, -6.338944243255235518E-49, 1.000000000000000000 ) ) ;
#1853=ORIENTED_EDGE ( 'NONE', *, *, #3450, .T. ) ;
#1861=ORIENTED_EDGE ( 'NONE', *, *, #8921, .T. ) ;
#1877=ORIENTED_EDGE ( 'NONE', *, *, #1055, .T. ) ;
#1893=FACE_OUTER_BOUND ( 'NONE', #8859, .T. ) ;
#1901=DIRECTION ( 'NONE',  ( 1.000000000000000000, 0.000000000000000000, 0.000000000000000000 ) ) ;
#1932=EDGE_CURVE ( 'NONE', #2493, #4771, #5404, .T. ) ;
#1933=AXIS2_PLACEMENT_3D ( 'NONE', #677, #4554, #5320 ) ;
#1939=DIRECTION ( 'NONE',  ( 0.000000000000000000, -6.338944243255235518E-49, 1.000000000000000000 ) ) ;
#1962=CARTESIAN_POINT ( 'NONE',  ( -4.246973736992222470, -14.10948682827616096, -1.270000000000007123 ) ) ;
#1968=SHAPE_REPRESENTATION_RELATIONSHIP ( 'NONE' , 'NONE' ,  #1047, #2769 ) ;
#2063=ORIENTED_EDGE ( 'NONE', *, *, #3301, .F. ) ;
#2116=FACE_OUTER_BOUND ( 'NONE', #145, .T. ) ;
#2153=AXIS2_PLACEMENT_3D ( 'NONE', #3378, #1776, #9689 ) ;
#2172=CIRCLE ( 'NONE', #2494, 15.44569104238500046 ) ;
#2174=CIRCLE ( 'NONE', #3483, 0.9906000000000003691 ) ;
#2198=DIRECTION ( 'NONE',  ( 0.9575619921529161527, -0.2882273949230689802, 3.311798021194119518E-34 ) ) ;
#2200=DIRECTION ( 'NONE',  ( 1.000000000000000000, 0.000000000000000000, 0.000000000000000000 ) ) ;
#2244=CYLINDRICAL_SURFACE ( 'NONE', #10022, 1.816100000000000270 ) ;
#2247=LINE ( 'NONE', #22, #4477 ) ;
#2258=VERTEX_POINT ( 'NONE', #3281 ) ;
#2260=EDGE_CURVE ( 'NONE', #7109, #7986, #7260, .T. ) ;
#2322=EDGE_LOOP ( 'NONE', ( #3299, #2334, #4781, #8008 ) ) ;
#2331=FACE_OUTER_BOUND ( 'NONE', #6749, .T. ) ;
#2332=STYLED_ITEM ( 'NONE', ( #9456 ), #7008 ) ;
#2334=ORIENTED_EDGE ( 'NONE', *, *, #7588, .F. ) ;
#2349=CYLINDRICAL_SURFACE ( 'NONE', #5335, 17.72919999999999874 ) ;
#2353=CARTESIAN_POINT ( 'NONE',  ( 11.48991645990273724, -11.34085470199652512, -1.270000000000007123 ) ) ;
#2372=CARTESIAN_POINT ( 'NONE',  ( 0.000000000000000000, -1.018491042385001544, 0.000000000000000000 ) ) ;
#2378=EDGE_CURVE ( 'NONE', #728, #3550, #1331, .T. ) ;
#2386=CARTESIAN_POINT ( 'NONE',  ( 6.976602070941136269, -13.58603705635637304, -1.270000000000007123 ) ) ;
#2393=EDGE_LOOP ( 'NONE', ( #702, #4065, #7859, #9267 ) ) ;
#2421=ORIENTED_EDGE ( 'NONE', *, *, #1932, .T. ) ;
#2423=ORIENTED_EDGE ( 'NONE', *, *, #1818, .T. ) ;
#2429=DIRECTION ( 'NONE',  ( 1.000000000000000000, 0.000000000000000000, 0.000000000000000000 ) ) ;
#2431=ORIENTED_EDGE ( 'NONE', *, *, #9868, .F. ) ;
#2453=ADVANCED_FACE ( 'NONE', ( #390 ), #2856, .F. ) ;
#2466=LINE ( 'NONE', #6532, #6097 ) ;
#2487=CIRCLE ( 'NONE', #1507, 0.9906000000000003691 ) ;
#2493=VERTEX_POINT ( 'NONE', #5898 ) ;
#2494=AXIS2_PLACEMENT_3D ( 'NONE', #5346, #6877, #8603 ) ;
#2502=DIRECTION ( 'NONE',  ( 0.000000000000000000, -6.338944243255235518E-49, 1.000000000000000000 ) ) ;
#2512=FILL_AREA_STYLE ('',( #5512 ) ) ;
#2520=CARTESIAN_POINT ( 'NONE',  ( -15.44569104238500046, -1.018491042384999545, 1.237085481564325490E-63 ) ) ;
#2531=DIRECTION ( 'NONE',  ( 0.000000000000000000, 6.338944243255235518E-49, -1.000000000000000000 ) ) ;
#2541=EDGE_CURVE ( 'NONE', #3552, #7029, #2645, .T. ) ;
#2543=DIRECTION ( 'NONE',  ( 0.000000000000000000, -6.338944243255235518E-49, 1.000000000000000000 ) ) ;
#2558=ORIENTED_EDGE ( 'NONE', *, *, #6528, .T. ) ;
#2565=DIRECTION ( 'NONE',  ( 0.000000000000000000, -6.338944243255235518E-49, 1.000000000000000000 ) ) ;
#2641=DIRECTION ( 'NONE',  ( 0.000000000000000000, -6.338944243255235518E-49, 1.000000000000000000 ) ) ;
#2645=CIRCLE ( 'NONE', #10085, 17.72919999999999874 ) ;
#2654=VECTOR ( 'NONE', #3460, 1000.000000000000000 ) ;
#2655=VERTEX_POINT ( 'NONE', #7565 ) ;
#2679=EDGE_CURVE ( 'NONE', #4852, #94, #1162, .T. ) ;
#2729=CARTESIAN_POINT ( 'NONE',  ( -4.169902070941136074, -13.58603705635637482, -1.270000000000007123 ) ) ;
#2736=( NAMED_UNIT ( * ) SI_UNIT ( $, .STERADIAN. ) SOLID_ANGLE_UNIT ( ) );
#2743=EDGE_CURVE ( 'NONE', #9801, #5925, #4462, .T. ) ;
#2769=ADVANCED_BREP_SHAPE_REPRESENTATION ( '', ( #7008, #3995 ), #7950 ) ;
#2774=PRODUCT_CONTEXT ( 'NONE', #5395, 'mechanical' ) ;
#2776=ORIENTED_EDGE ( 'NONE', *, *, #7726, .F. ) ;
#2788=ORIENTED_EDGE ( 'NONE', *, *, #6539, .T. ) ;
#2795=CIRCLE ( 'NONE', #3809, 17.72919999999999874 ) ;
#2812=EDGE_CURVE ( 'NONE', #6711, #7540, #2172, .T. ) ;
#2822=ORIENTED_EDGE ( 'NONE', *, *, #5504, .F. ) ;
#2831=AXIS2_PLACEMENT_3D ( 'NONE', #2976, #9242, #6952 ) ;
#2847=ADVANCED_FACE ( 'NONE', ( #6990 ), #1475, .T. ) ;
#2856=CYLINDRICAL_SURFACE ( 'NONE', #841, 0.9906000000000003691 ) ;
#2866=VECTOR ( 'NONE', #6199, 1000.000000000000000 ) ;
#2896=PLANE ( 'NONE',  #885 ) ;
#2924=CARTESIAN_POINT ( 'NONE',  ( -4.995402070941133310, -13.58603705635637304, 0.000000000000000000 ) ) ;
#2936=FACE_OUTER_BOUND ( 'NONE', #6556, .T. ) ;
#2946=ORIENTED_EDGE ( 'NONE', *, *, #8692, .F. ) ;
#2976=CARTESIAN_POINT ( 'NONE',  ( 0.000000000000000000, 0.000000000000000000, 0.000000000000000000 ) ) ;
#2999=CARTESIAN_POINT ( 'NONE',  ( -5.986002070941136566, -13.58603705635637482, -1.270000000000007123 ) ) ;
#3005=AXIS2_PLACEMENT_3D ( 'NONE', #2372, #1708, #883 ) ;
#3006=DIRECTION ( 'NONE',  ( 0.000000000000000000, -6.338944243255235518E-49, 1.000000000000000000 ) ) ;
#3012=ORIENTED_EDGE ( 'NONE', *, *, #9611, .F. ) ;
#3020=CARTESIAN_POINT ( 'NONE',  ( -15.44569104238500046, -1.018491042384999545, -1.270000000000007123 ) ) ;
#3063=VERTEX_POINT ( 'NONE', #9285 ) ;
#3080=ADVANCED_FACE ( 'NONE', ( #9334 ), #2244, .T. ) ;
#3129=EDGE_CURVE ( 'NONE', #7109, #6243, #9033, .T. ) ;
#3154=AXIS2_PLACEMENT_3D ( 'NONE', #889, #2531, #2429 ) ;
#3176=CARTESIAN_POINT ( 'NONE',  ( -1.925929944387235853E-31, -1.018491042385001544, -1.270000000000007123 ) ) ;
#3224=PLANE ( 'NONE',  #4494 ) ;
#3225=DIRECTION ( 'NONE',  ( 0.000000000000000000, 6.338944243255235518E-49, -1.000000000000000000 ) ) ;
#3266=( LENGTH_UNIT ( ) NAMED_UNIT ( * ) SI_UNIT ( .MILLI., .METRE. ) );
#3275=FACE_OUTER_BOUND ( 'NONE', #3849, .T. ) ;
#3281=CARTESIAN_POINT ( 'NONE',  ( -11.48991645990274257, -11.34085470199651979, 0.000000000000000000 ) ) ;
#3296=ORIENTED_EDGE ( 'NONE', *, *, #9611, .T. ) ;
#3299=ORIENTED_EDGE ( 'NONE', *, *, #1473, .F. ) ;
#3301=EDGE_CURVE ( 'NONE', #94, #4710, #5720, .T. ) ;
#3303=CIRCLE ( 'NONE', #9085, 3.632199999999998763 ) ;
#3378=CARTESIAN_POINT ( 'NONE',  ( -5.986002070941133901, -13.58603705635637304, -1.270000000000007123 ) ) ;
#3399=ORIENTED_EDGE ( 'NONE', *, *, #10144, .T. ) ;
#3410=CARTESIAN_POINT ( 'NONE',  ( -8.787954181158717404, -8.913453481710840620, -1.270000000000007123 ) ) ;
#3450=EDGE_CURVE ( 'NONE', #5925, #8713, #8033, .T. ) ;
#3460=DIRECTION ( 'NONE',  ( 0.000000000000000000, -6.338944243255235518E-49, 1.000000000000000000 ) ) ;
#3474=AXIS2_PLACEMENT_3D ( 'NONE', #7413, #341, #6621 ) ;
#3483=AXIS2_PLACEMENT_3D ( 'NONE', #188, #2565, #8874 ) ;
#3485=EDGE_CURVE ( 'NONE', #4710, #94, #4574, .T. ) ;
#3491=CARTESIAN_POINT ( 'NONE',  ( 5.110041130070070992, -16.97680807127747826, -1.270000000000007123 ) ) ;
#3505=ORIENTED_EDGE ( 'NONE', *, *, #1061, .T. ) ;
#3509=EDGE_CURVE ( 'NONE', #5109, #1717, #3787, .T. ) ;
#3524=( LENGTH_UNIT ( ) NAMED_UNIT ( * ) SI_UNIT ( .MILLI., .METRE. ) );
#3538=ORIENTED_EDGE ( 'NONE', *, *, #5805, .F. ) ;
#3550=VERTEX_POINT ( 'NONE', #5978 ) ;
#3552=VERTEX_POINT ( 'NONE', #3608 ) ;
#3560=LINE ( 'NONE', #2729, #5992 ) ;
#3574=DIRECTION ( 'NONE',  ( 1.000000000000000000, 0.000000000000000000, 0.000000000000000000 ) ) ;
#3580=ORIENTED_EDGE ( 'NONE', *, *, #9373, .F. ) ;
#3584=DIRECTION ( 'NONE',  ( 0.000000000000000000, -6.338944243255235518E-49, 1.000000000000000000 ) ) ;
#3587=UNCERTAINTY_MEASURE_WITH_UNIT (LENGTH_MEASURE( 1.000000000000000082E-05 ), #7262, 'distance_accuracy_value', 'NONE');
#3608=CARTESIAN_POINT ( 'NONE',  ( 5.110041130070070992, -16.97680807127747826, -1.270000000000007123 ) ) ;
#3626=EDGE_CURVE ( 'NONE', #8713, #6711, #3752, .T. ) ;
#3632=CIRCLE ( 'NONE', #9430, 1.816100000000000270 ) ;
#3673=CARTESIAN_POINT ( 'NONE',  ( -15.44569104238500046, -1.018491042384999545, -1.270000000000007123 ) ) ;
#3693=DIRECTION ( 'NONE',  ( 0.000000000000000000, -6.338944243255235518E-49, 1.000000000000000000 ) ) ;
#3738=EDGE_CURVE ( 'NONE', #1717, #273, #5826, .T. ) ;
#3752=CIRCLE ( 'NONE', #9536, 3.632200000000000539 ) ;
#3755=ORIENTED_EDGE ( 'NONE', *, *, #6995, .T. ) ;
#3781=CARTESIAN_POINT ( 'NONE',  ( -4.246973736992222470, -14.10948682827616096, -1.270000000000007123 ) ) ;
#3783=ADVANCED_FACE ( 'NONE', ( #2116 ), #3827, .F. ) ;
#3784=ORIENTED_EDGE ( 'NONE', *, *, #417, .F. ) ;
#3787=LINE ( 'NONE', #9424, #4904 ) ;
#3796=ORIENTED_EDGE ( 'NONE', *, *, #8259, .T. ) ;
#3798=CARTESIAN_POINT ( 'NONE',  ( -5.986002070941136566, -13.58603705635637482, -1.270000000000007123 ) ) ;
#3805=DIRECTION ( 'NONE',  ( 1.000000000000000000, 0.000000000000000000, 0.000000000000000000 ) ) ;
#3809=AXIS2_PLACEMENT_3D ( 'NONE', #3984, #683, #1560 ) ;
#3827=CYLINDRICAL_SURFACE ( 'NONE', #1933, 0.9906000000000003691 ) ;
#3849=EDGE_LOOP ( 'NONE', ( #8264, #8474, #738, #9255 ) ) ;
#3853=FACE_OUTER_BOUND ( 'NONE', #2322, .T. ) ;
#3902=DIRECTION ( 'NONE',  ( 0.000000000000000000, -6.338944243255235518E-49, 1.000000000000000000 ) ) ;
#3919=CIRCLE ( 'NONE', #623, 17.72919999999999874 ) ;
#3921=EDGE_LOOP ( 'NONE', ( #2431, #1067, #5523, #7212 ) ) ;
#3945=ORIENTED_EDGE ( 'NONE', *, *, #9868, .T. ) ;
#3949=DIRECTION ( 'NONE',  ( 1.000000000000000000, 0.000000000000000000, 0.000000000000000000 ) ) ;
#3984=CARTESIAN_POINT ( 'NONE',  ( 0.000000000000000000, 0.000000000000000000, 0.000000000000000000 ) ) ;
#3991=ORIENTED_EDGE ( 'NONE', *, *, #2679, .T. ) ;
#3993=ADVANCED_FACE ( 'NONE', ( #2936 ), #6026, .T. ) ;
#3995=AXIS2_PLACEMENT_3D ( 'NONE', #245, #8930, #7419 ) ;
#4002=ORIENTED_EDGE ( 'NONE', *, *, #3738, .F. ) ;
#4003=CIRCLE ( 'NONE', #3005, 15.44569104238500046 ) ;
#4006=FACE_OUTER_BOUND ( 'NONE', #10045, .T. ) ;
#4015=CARTESIAN_POINT ( 'NONE',  ( 5.986002070941135678, -13.58603705635637304, 0.000000000000000000 ) ) ;
#4040=ORIENTED_EDGE ( 'NONE', *, *, #3485, .F. ) ;
#4051=DIRECTION ( 'NONE',  ( 1.000000000000000000, 0.000000000000000000, 0.000000000000000000 ) ) ;
#4065=ORIENTED_EDGE ( 'NONE', *, *, #10020, .T. ) ;
#4074=DIRECTION ( 'NONE',  ( 0.000000000000000000, -6.338944243255235518E-49, 1.000000000000000000 ) ) ;
#4082=ADVANCED_FACE ( 'NONE', ( #7899 ), #775, .F. ) ;
#4084=AXIS2_PLACEMENT_3D ( 'NONE', #5623, #7129, #45 ) ;
#4116=CARTESIAN_POINT ( 'NONE',  ( 17.72919999999999874, -4.025229594467075325E-49, -1.270000000000007123 ) ) ;
#4138=VECTOR ( 'NONE', #7969, 1000.000000000000000 ) ;
#4146=CARTESIAN_POINT ( 'NONE',  ( -11.48991645990274257, -11.34085470199651979, -1.270000000000007123 ) ) ;
#4159=CLOSED_SHELL ( 'NONE', ( #867, #2453, #9601, #903, #8311, #4969, #1495, #8034, #7277, #3993, #5127, #4712, #4082, #3080, #2847, #5656, #5169, #5270, #3783 ) ) ;
#4161=EDGE_CURVE ( 'NONE', #4954, #8895, #3919, .T. ) ;
#4199=DIRECTION ( 'NONE',  ( 0.000000000000000000, -6.338944243255235518E-49, 1.000000000000000000 ) ) ;
#4202=CARTESIAN_POINT ( 'NONE',  ( -1.925929944387235853E-31, -1.018491042385001544, -1.270000000000007123 ) ) ;
#4216=UNCERTAINTY_MEASURE_WITH_UNIT (LENGTH_MEASURE( 1.000000000000000082E-05 ), #3524, 'distance_accuracy_value', 'NONE');
#4224=DIRECTION ( 'NONE',  ( 1.000000000000000000, 0.000000000000000000, 0.000000000000000000 ) ) ;
#4252=CYLINDRICAL_SURFACE ( 'NONE', #2153, 0.9906000000000003691 ) ;
#4270=EDGE_CURVE ( 'NONE', #1499, #3063, #4003, .T. ) ;
#4282=ORIENTED_EDGE ( 'NONE', *, *, #429, .F. ) ;
#4293=( NAMED_UNIT ( * ) SI_UNIT ( $, .STERADIAN. ) SOLID_ANGLE_UNIT ( ) );
#4309=AXIS2_PLACEMENT_3D ( 'NONE', #6311, #10154, #3949 ) ;
#4314=DIRECTION ( 'NONE',  ( 0.000000000000000000, -6.338944243255235518E-49, 1.000000000000000000 ) ) ;
#4367=CARTESIAN_POINT ( 'NONE',  ( 6.919986107680329290, -12.02850919814119379, -1.270000000000007123 ) ) ;
#4387=EDGE_LOOP ( 'NONE', ( #3755, #930 ) ) ;
#4399=FILL_AREA_STYLE_COLOUR ( '', #6125 ) ;
#4410=DIRECTION ( 'NONE',  ( 0.000000000000000000, -6.338944243255235518E-49, 1.000000000000000000 ) ) ;
#4432=ORIENTED_EDGE ( 'NONE', *, *, #7927, .F. ) ;
#4462=CIRCLE ( 'NONE', #8425, 1.816100000000000270 ) ;
#4469=CARTESIAN_POINT ( 'NONE',  ( 4.246973736992224246, -14.10948682827615919, 0.000000000000000000 ) ) ;
#4477=VECTOR ( 'NONE', #3902, 1000.000000000000000 ) ;
#4494=AXIS2_PLACEMENT_3D ( 'NONE', #1579, #4577, #6161 ) ;
#4496=AXIS2_PLACEMENT_3D ( 'NONE', #9182, #3584, #6110 ) ;
#4500=CARTESIAN_POINT ( 'NONE',  ( 5.986002070941135678, -13.58603705635637304, -1.270000000000007123 ) ) ;
#4509=VECTOR ( 'NONE', #586, 1000.000000000000000 ) ;
#4513=FACE_BOUND ( 'NONE', #6385, .T. ) ;
#4531=DIRECTION ( 'NONE',  ( 0.000000000000000000, 6.338944243255235518E-49, -1.000000000000000000 ) ) ;
#4544=EDGE_CURVE ( 'NONE', #7640, #7109, #1359, .T. ) ;
#4549=EDGE_CURVE ( 'NONE', #1309, #9252, #7106, .T. ) ;
#4553=ORIENTED_EDGE ( 'NONE', *, *, #9373, .T. ) ;
#4554=DIRECTION ( 'NONE',  ( 0.000000000000000000, -6.338944243255235518E-49, 1.000000000000000000 ) ) ;
#4561=CARTESIAN_POINT ( 'NONE',  ( -1.925929944387235853E-31, -1.018491042385001544, -1.270000000000007123 ) ) ;
#4574=CIRCLE ( 'NONE', #283, 0.9906000000000003691 ) ;
#4577=DIRECTION ( 'NONE',  ( 0.000000000000000000, -6.338944243255235518E-49, 1.000000000000000000 ) ) ;
#4621=ORIENTED_EDGE ( 'NONE', *, *, #7934, .F. ) ;
#4623=DIRECTION ( 'NONE',  ( 0.000000000000000000, -6.338944243255235518E-49, 1.000000000000000000 ) ) ;
#4677=CYLINDRICAL_SURFACE ( 'NONE', #4309, 3.632199999999998763 ) ;
#4678=CARTESIAN_POINT ( 'NONE',  ( 4.995402070941135086, -13.58603705635637304, 0.000000000000000000 ) ) ;
#4710=VERTEX_POINT ( 'NONE', #9954 ) ;
#4712=ADVANCED_FACE ( 'NONE', ( #7330 ), #5236, .F. ) ;
#4725=DIRECTION ( 'NONE',  ( 1.000000000000000000, 0.000000000000000000, 0.000000000000000000 ) ) ;
#4727=FACE_OUTER_BOUND ( 'NONE', #6222, .T. ) ;
#4741=AXIS2_PLACEMENT_3D ( 'NONE', #7246, #4199, #4051 ) ;
#4759=LINE ( 'NONE', #6140, #6737 ) ;
#4771=VERTEX_POINT ( 'NONE', #253 ) ;
#4781=ORIENTED_EDGE ( 'NONE', *, *, #4544, .T. ) ;
#4808=LINE ( 'NONE', #51, #6275 ) ;
#4809=CIRCLE ( 'NONE', #7088, 15.44569104238500046 ) ;
#4819=CARTESIAN_POINT ( 'NONE',  ( -4.169902070941136074, -13.58603705635637482, 0.000000000000000000 ) ) ;
#4822=ORIENTED_EDGE ( 'NONE', *, *, #3450, .F. ) ;
#4850=VERTEX_POINT ( 'NONE', #4469 ) ;
#4852=VERTEX_POINT ( 'NONE', #598 ) ;
#4899=DIRECTION ( 'NONE',  ( 0.2882273949230689802, 0.9575619921529161527, -1.755378125195851735E-33 ) ) ;
#4904=VECTOR ( 'NONE', #9324, 1000.000000000000000 ) ;
#4916=CARTESIAN_POINT ( 'NONE',  ( 11.48991645990273724, -11.34085470199652512, 0.000000000000000000 ) ) ;
#4932=DIRECTION ( 'NONE',  ( 1.000000000000000000, 0.000000000000000000, 0.000000000000000000 ) ) ;
#4936=ORIENTED_EDGE ( 'NONE', *, *, #6195, .F. ) ;
#4954=VERTEX_POINT ( 'NONE', #9442 ) ;
#4969=ADVANCED_FACE ( 'NONE', ( #4727 ), #2349, .T. ) ;
#4984=DIRECTION ( 'NONE',  ( 0.000000000000000000, -6.338944243255235518E-49, 1.000000000000000000 ) ) ;
#5033=FACE_OUTER_BOUND ( 'NONE', #3921, .T. ) ;
#5039=CARTESIAN_POINT ( 'NONE',  ( 6.919986107680329290, -12.02850919814119379, -1.270000000000007123 ) ) ;
#5042=PLANE ( 'NONE',  #3474 ) ;
#5050=FACE_OUTER_BOUND ( 'NONE', #2393, .T. ) ;
#5054=ORIENTED_EDGE ( 'NONE', *, *, #1535, .F. ) ;
#5074=FACE_BOUND ( 'NONE', #4387, .T. ) ;
#5109=VERTEX_POINT ( 'NONE', #800 ) ;
#5111=DIRECTION ( 'NONE',  ( 0.000000000000000000, -6.338944243255235518E-49, 1.000000000000000000 ) ) ;
#5119=AXIS2_PLACEMENT_3D ( 'NONE', #6365, #4984, #5698 ) ;
#5127=ADVANCED_FACE ( 'NONE', ( #3853 ), #4677, .F. ) ;
#5169=ADVANCED_FACE ( 'NONE', ( #7045, #7921, #4006 ), #3224, .T. ) ;
#5175=CARTESIAN_POINT ( 'NONE',  ( 6.976602070941136269, -13.58603705635637304, -1.270000000000007123 ) ) ;
#5236=CYLINDRICAL_SURFACE ( 'NONE', #4496, 15.44569104238500046 ) ;
#5247=ORIENTED_EDGE ( 'NONE', *, *, #2743, .F. ) ;
#5270=ADVANCED_FACE ( 'NONE', ( #6559 ), #119, .F. ) ;
#5320=DIRECTION ( 'NONE',  ( 1.000000000000000000, 0.000000000000000000, 0.000000000000000000 ) ) ;
#5334=DIRECTION ( 'NONE',  ( 1.000000000000000000, 0.000000000000000000, 0.000000000000000000 ) ) ;
#5335=AXIS2_PLACEMENT_3D ( 'NONE', #8705, #7094, #2200 ) ;
#5344=ORIENTED_EDGE ( 'NONE', *, *, #6195, .T. ) ;
#5346=CARTESIAN_POINT ( 'NONE',  ( -1.925929944387235853E-31, -1.018491042385001544, -1.270000000000007123 ) ) ;
#5395=APPLICATION_CONTEXT ( 'automotive_design' ) ;
#5404=LINE ( 'NONE', #1435, #9092 ) ;
#5461=COLOUR_RGB ( '', 0.66274510, 0.83137255, 0.94901961) ;
#5481=DIRECTION ( 'NONE',  ( 0.000000000000000000, -6.338944243255235518E-49, 1.000000000000000000 ) ) ;
#5494=VECTOR ( 'NONE', #1454, 1000.000000000000000 ) ;
#5504=EDGE_CURVE ( 'NONE', #3063, #6295, #8470, .T. ) ;
#5512=FILL_AREA_STYLE_COLOUR ( '', #5461 ) ;
#5523=ORIENTED_EDGE ( 'NONE', *, *, #417, .T. ) ;
#5601=ORIENTED_EDGE ( 'NONE', *, *, #7907, .T. ) ;
#5613=CIRCLE ( 'NONE', #9922, 1.816100000000000270 ) ;
#5623=CARTESIAN_POINT ( 'NONE',  ( -8.787954181158717404, -8.913453481710840620, -1.270000000000007123 ) ) ;
#5647=DIRECTION ( 'NONE',  ( 1.000000000000000000, 0.000000000000000000, 0.000000000000000000 ) ) ;
#5648=DIRECTION ( 'NONE',  ( 1.000000000000000000, 0.000000000000000000, 0.000000000000000000 ) ) ;
#5656=ADVANCED_FACE ( 'NONE', ( #4513, #5074, #9942 ), #2896, .F. ) ;
#5661=SURFACE_STYLE_FILL_AREA ( #2512 ) ;
#5673=ORIENTED_EDGE ( 'NONE', *, *, #1055, .F. ) ;
#5687=DIRECTION ( 'NONE',  ( 1.000000000000000000, 0.000000000000000000, 0.000000000000000000 ) ) ;
#5692=CARTESIAN_POINT ( 'NONE',  ( -5.986002070941136566, -13.58603705635637482, -1.270000000000007123 ) ) ;
#5698=DIRECTION ( 'NONE',  ( 1.000000000000000000, 0.000000000000000000, 0.000000000000000000 ) ) ;
#5706=( NAMED_UNIT ( * ) SI_UNIT ( $, .STERADIAN. ) SOLID_ANGLE_UNIT ( ) );
#5720=CIRCLE ( 'NONE', #6867, 0.9906000000000003691 ) ;
#5728=ORIENTED_EDGE ( 'NONE', *, *, #1473, .T. ) ;
#5764=ORIENTED_EDGE ( 'NONE', *, *, #4544, .F. ) ;
#5783=( GEOMETRIC_REPRESENTATION_CONTEXT ( 3 ) GLOBAL_UNCERTAINTY_ASSIGNED_CONTEXT ( ( #3587 ) ) GLOBAL_UNIT_ASSIGNED_CONTEXT ( ( #7262, #1591, #5706 ) ) REPRESENTATION_CONTEXT ( 'NONE', 'WORKASPACE' ) );
#5784=VECTOR ( 'NONE', #6807, 1000.000000000000000 ) ;
#5785=CARTESIAN_POINT ( 'NONE',  ( -6.919986107680330178, -12.02850919814119557, -1.270000000000007123 ) ) ;
#5805=EDGE_CURVE ( 'NONE', #1309, #728, #6656, .T. ) ;
#5816=VERTEX_POINT ( 'NONE', #428 ) ;
#5819=ORIENTED_EDGE ( 'NONE', *, *, #100, .F. ) ;
#5826=LINE ( 'NONE', #10178, #1449 ) ;
#5849=DIRECTION ( 'NONE',  ( 1.000000000000000000, 0.000000000000000000, 0.000000000000000000 ) ) ;
#5851=LINE ( 'NONE', #9028, #9265 ) ;
#5862=ORIENTED_EDGE ( 'NONE', *, *, #2378, .T. ) ;
#5871=ORIENTED_EDGE ( 'NONE', *, *, #6995, .F. ) ;
#5873=ORIENTED_EDGE ( 'NONE', *, *, #6843, .T. ) ;
#5887=CARTESIAN_POINT ( 'NONE',  ( 0.000000000000000000, 0.000000000000000000, -1.270000000000007123 ) ) ;
#5898=CARTESIAN_POINT ( 'NONE',  ( -17.72919999999999874, 2.171200803144325526E-15, -1.270000000000007123 ) ) ;
#5925=VERTEX_POINT ( 'NONE', #1464 ) ;
#5940=VECTOR ( 'NONE', #9447, 1000.000000000000114 ) ;
#5978=CARTESIAN_POINT ( 'NONE',  ( 6.976602070941136269, -13.58603705635637304, 0.000000000000000000 ) ) ;
#5988=ORIENTED_EDGE ( 'NONE', *, *, #8921, .F. ) ;
#5992=VECTOR ( 'NONE', #6643, 1000.000000000000000 ) ;
#6004=CARTESIAN_POINT ( 'NONE',  ( -4.246973736992222470, -14.10948682827616096, 0.000000000000000000 ) ) ;
#6015=ORIENTED_EDGE ( 'NONE', *, *, #4161, .T. ) ;
#6023=EDGE_CURVE ( 'NONE', #2493, #5109, #8152, .T. ) ;
#6025=ORIENTED_EDGE ( 'NONE', *, *, #7934, .T. ) ;
#6026=CYLINDRICAL_SURFACE ( 'NONE', #9864, 1.816100000000000270 ) ;
#6049=ORIENTED_EDGE ( 'NONE', *, *, #5504, .T. ) ;
#6097=VECTOR ( 'NONE', #4899, 999.9999999999998863 ) ;
#6103=ORIENTED_EDGE ( 'NONE', *, *, #7927, .T. ) ;
#6110=DIRECTION ( 'NONE',  ( 1.000000000000000000, 0.000000000000000000, 0.000000000000000000 ) ) ;
#6125=COLOUR_RGB ( '', 0.66274510, 0.83137255, 0.94901961) ;
#6140=CARTESIAN_POINT ( 'NONE',  ( 5.110041130070070992, -16.97680807127747826, 0.000000000000000000 ) ) ;
#6161=DIRECTION ( 'NONE',  ( 1.000000000000000000, 0.000000000000000000, 0.000000000000000000 ) ) ;
#6166=DIRECTION ( 'NONE',  ( 1.000000000000000000, 0.000000000000000000, 0.000000000000000000 ) ) ;
#6195=EDGE_CURVE ( 'NONE', #9252, #3550, #9374, .T. ) ;
#6199=DIRECTION ( 'NONE',  ( 0.000000000000000000, -6.338944243255235518E-49, 1.000000000000000000 ) ) ;
#6222=EDGE_LOOP ( 'NONE', ( #3796, #2421, #5819, #8936 ) ) ;
#6243=VERTEX_POINT ( 'NONE', #8012 ) ;
#6265=VECTOR ( 'NONE', #8185, 1000.000000000000000 ) ;
#6275=VECTOR ( 'NONE', #5481, 1000.000000000000000 ) ;
#6289=DIRECTION ( 'NONE',  ( 0.2882273949230682586, -0.9575619921529162637, -1.755378125195845577E-33 ) ) ;
#6295=VERTEX_POINT ( 'NONE', #4916 ) ;
#6309=DIRECTION ( 'NONE',  ( 0.2882273949230689802, 0.9575619921529161527, -1.755378125195851735E-33 ) ) ;
#6311=CARTESIAN_POINT ( 'NONE',  ( 8.787954181158717404, -8.913453481710838844, -1.270000000000007123 ) ) ;
#6312=DIRECTION ( 'NONE',  ( 1.000000000000000000, 0.000000000000000000, 0.000000000000000000 ) ) ;
#6315=CARTESIAN_POINT ( 'NONE',  ( 0.000000000000000000, -1.018491042385001544, 0.000000000000000000 ) ) ;
#6365=CARTESIAN_POINT ( 'NONE',  ( 0.000000000000000000, 0.000000000000000000, -1.270000000000007123 ) ) ;
#6385=EDGE_LOOP ( 'NONE', ( #9976, #8103 ) ) ;
#6416=CYLINDRICAL_SURFACE ( 'NONE', #5119, 17.72919999999999874 ) ;
#6440=EDGE_LOOP ( 'NONE', ( #9358, #3580, #7339, #356 ) ) ;
#6486=CARTESIAN_POINT ( 'NONE',  ( 8.787954181158717404, -8.913453481710838844, 0.000000000000000000 ) ) ;
#6514=CARTESIAN_POINT ( 'NONE',  ( 6.919986107680329290, -12.02850919814119379, 0.000000000000000000 ) ) ;
#6528=EDGE_CURVE ( 'NONE', #5925, #8732, #3560, .T. ) ;
#6532=CARTESIAN_POINT ( 'NONE',  ( -5.110041130070070992, -16.97680807127747826, -1.270000000000007123 ) ) ;
#6539=EDGE_CURVE ( 'NONE', #9801, #273, #9979, .T. ) ;
#6545=DIRECTION ( 'NONE',  ( 1.000000000000000000, 0.000000000000000000, 0.000000000000000000 ) ) ;
#6556=EDGE_LOOP ( 'NONE', ( #9551, #1386, #1273, #455 ) ) ;
#6559=FACE_OUTER_BOUND ( 'NONE', #6892, .T. ) ;
#6587=AXIS2_PLACEMENT_3D ( 'NONE', #8195, #4074, #4224 ) ;
#6606=MECHANICAL_DESIGN_GEOMETRIC_PRESENTATION_REPRESENTATION('',(#1690),#8051);
#6621=DIRECTION ( 'NONE',  ( 0.2882273949230683141, -0.9575619921529162637, -1.755378125195845919E-33 ) ) ;
#6643=DIRECTION ( 'NONE',  ( 0.000000000000000000, -6.338944243255235518E-49, 1.000000000000000000 ) ) ;
#6650=( NAMED_UNIT ( * ) PLANE_ANGLE_UNIT ( ) SI_UNIT ( $, .RADIAN. ) );
#6656=LINE ( 'NONE', #532, #4509 ) ;
#6702=DIRECTION ( 'NONE',  ( 0.000000000000000000, -6.338944243255235518E-49, 1.000000000000000000 ) ) ;
#6711=VERTEX_POINT ( 'NONE', #8209 ) ;
#6714=DIRECTION ( 'NONE',  ( 1.000000000000000000, 0.000000000000000000, 0.000000000000000000 ) ) ;
#6737=VECTOR ( 'NONE', #6289, 1000.000000000000114 ) ;
#6747=CIRCLE ( 'NONE', #6932, 0.9906000000000003691 ) ;
#6748=CIRCLE ( 'NONE', #8254, 17.72919999999999874 ) ;
#6749=EDGE_LOOP ( 'NONE', ( #9641, #2558, #5988, #6765 ) ) ;
#6765=ORIENTED_EDGE ( 'NONE', *, *, #6539, .F. ) ;
#6807=DIRECTION ( 'NONE',  ( 0.000000000000000000, -6.338944243255235518E-49, 1.000000000000000000 ) ) ;
#6825=CARTESIAN_POINT ( 'NONE',  ( 5.986002070941135678, -13.58603705635637304, -1.270000000000007123 ) ) ;
#6843=EDGE_CURVE ( 'NONE', #285, #4710, #8636, .T. ) ;
#6867=AXIS2_PLACEMENT_3D ( 'NONE', #7919, #7300, #9642 ) ;
#6877=DIRECTION ( 'NONE',  ( 0.000000000000000000, 6.338944243255235518E-49, -1.000000000000000000 ) ) ;
#6885=CARTESIAN_POINT ( 'NONE',  ( -5.986002070941133901, -13.58603705635637304, -1.270000000000007123 ) ) ;
#6887=PRODUCT_DEFINITION_FORMATION_WITH_SPECIFIED_SOURCE ( 'ANY', '', #7484, .NOT_KNOWN. ) ;
#6892=EDGE_LOOP ( 'NONE', ( #3538, #5871, #5344, #5601 ) ) ;
#6932=AXIS2_PLACEMENT_3D ( 'NONE', #6885, #7788, #10158 ) ;
#6941=CARTESIAN_POINT ( 'NONE',  ( 5.110041130070070992, -16.97680807127747826, -1.270000000000007123 ) ) ;
#6952=DIRECTION ( 'NONE',  ( 1.000000000000000000, 0.000000000000000000, 0.000000000000000000 ) ) ;
#6964=ORIENTED_EDGE ( 'NONE', *, *, #2541, .F. ) ;
#6972=DIRECTION ( 'NONE',  ( 1.000000000000000000, 0.000000000000000000, 0.000000000000000000 ) ) ;
#6990=FACE_OUTER_BOUND ( 'NONE', #7137, .T. ) ;
#6995=EDGE_CURVE ( 'NONE', #9252, #1309, #2174, .T. ) ;
#7008=MANIFOLD_SOLID_BREP ( 'Body', #4159 ) ;
#7018=ORIENTED_EDGE ( 'NONE', *, *, #7907, .F. ) ;
#7029=VERTEX_POINT ( 'NONE', #4116 ) ;
#7045=FACE_BOUND ( 'NONE', #8690, .T. ) ;
#7088=AXIS2_PLACEMENT_3D ( 'NONE', #3176, #3225, #6312 ) ;
#7094=DIRECTION ( 'NONE',  ( 0.000000000000000000, -6.338944243255235518E-49, 1.000000000000000000 ) ) ;
#7106=CIRCLE ( 'NONE', #531, 0.9906000000000003691 ) ;
#7109=VERTEX_POINT ( 'NONE', #4367 ) ;
#7129=DIRECTION ( 'NONE',  ( 0.000000000000000000, -6.338944243255235518E-49, 1.000000000000000000 ) ) ;
#7137=EDGE_LOOP ( 'NONE', ( #4002, #8251, #505, #2788 ) ) ;
#7212=ORIENTED_EDGE ( 'NONE', *, *, #4270, .F. ) ;
#7221=EDGE_CURVE ( 'NONE', #3552, #4954, #7519, .T. ) ;
#7235=ORIENTED_EDGE ( 'NONE', *, *, #8845, .F. ) ;
#7246=CARTESIAN_POINT ( 'NONE',  ( 5.986002070941135678, -13.58603705635637304, -1.270000000000007123 ) ) ;
#7252=PRODUCT_DEFINITION ( 'UNKNOWN', '', #6887, #8346 ) ;
#7260=LINE ( 'NONE', #5039, #6265 ) ;
#7262=( LENGTH_UNIT ( ) NAMED_UNIT ( * ) SI_UNIT ( .MILLI., .METRE. ) );
#7266=VECTOR ( 'NONE', #487, 1000.000000000000000 ) ;
#7268=AXIS2_PLACEMENT_3D ( 'NONE', #7295, #2543, #5687 ) ;
#7277=ADVANCED_FACE ( 'NONE', ( #1893 ), #5042, .T. ) ;
#7282=EDGE_CURVE ( 'NONE', #6243, #4850, #5851, .T. ) ;
#7295=CARTESIAN_POINT ( 'NONE',  ( -5.986002070941133901, -13.58603705635637304, -1.270000000000007123 ) ) ;
#7300=DIRECTION ( 'NONE',  ( 0.000000000000000000, -6.338944243255235518E-49, 1.000000000000000000 ) ) ;
#7330=FACE_OUTER_BOUND ( 'NONE', #7480, .T. ) ;
#7339=ORIENTED_EDGE ( 'NONE', *, *, #3626, .T. ) ;
#7353=DIRECTION ( 'NONE',  ( 1.000000000000000000, 0.000000000000000000, 0.000000000000000000 ) ) ;
#7375=EDGE_LOOP ( 'NONE', ( #9863, #1853, #4553, #4621 ) ) ;
#7394=PRESENTATION_STYLE_ASSIGNMENT (( #9009 ) ) ;
#7413=CARTESIAN_POINT ( 'NONE',  ( 5.110041130070070992, -16.97680807127747826, -1.270000000000007123 ) ) ;
#7419=DIRECTION ( 'NONE',  ( 1.000000000000000000, 0.000000000000000000, 0.000000000000000000 ) ) ;
#7464=CARTESIAN_POINT ( 'NONE',  ( -4.995402070941133310, -13.58603705635637304, -1.270000000000007123 ) ) ;
#7472=CARTESIAN_POINT ( 'NONE',  ( 17.72919999999999874, -4.025229594467098114E-49, 0.000000000000000000 ) ) ;
#7480=EDGE_LOOP ( 'NONE', ( #3784, #3296, #92, #2822 ) ) ;
#7484=PRODUCT ( 'basic internal retaining ring_ai_B27.1 - NA2-131', 'basic internal retaining ring_ai_B27.1 - NA2-131', '', ( #2774 ) ) ;
#7508=DIRECTION ( 'NONE',  ( 0.000000000000000000, -6.338944243255235518E-49, 1.000000000000000000 ) ) ;
#7519=LINE ( 'NONE', #3491, #8602 ) ;
#7540=VERTEX_POINT ( 'NONE', #3020 ) ;
#7552=DIRECTION ( 'NONE',  ( 0.000000000000000000, -6.338944243255235518E-49, 1.000000000000000000 ) ) ;
#7565=CARTESIAN_POINT ( 'NONE',  ( -6.919986107680330178, -12.02850919814119557, 0.000000000000000000 ) ) ;
#7567=CARTESIAN_POINT ( 'NONE',  ( 5.986002070941135678, -13.58603705635637304, -1.270000000000007123 ) ) ;
#7582=ORIENTED_EDGE ( 'NONE', *, *, #3485, .T. ) ;
#7588=EDGE_CURVE ( 'NONE', #7640, #6295, #9496, .T. ) ;
#7605=( NAMED_UNIT ( * ) PLANE_ANGLE_UNIT ( ) SI_UNIT ( $, .RADIAN. ) );
#7640=VERTEX_POINT ( 'NONE', #2353 ) ;
#7661=DIRECTION ( 'NONE',  ( 0.000000000000000000, 6.338944243255235518E-49, -1.000000000000000000 ) ) ;
#7695=ORIENTED_EDGE ( 'NONE', *, *, #3301, .T. ) ;
#7726=EDGE_CURVE ( 'NONE', #2258, #1499, #8095, .T. ) ;
#7734=CARTESIAN_POINT ( 'NONE',  ( -6.976602070941134492, -13.58603705635637304, -1.270000000000007123 ) ) ;
#7756=CARTESIAN_POINT ( 'NONE',  ( -6.976602070941134492, -13.58603705635637304, -1.270000000000007123 ) ) ;
#7772=AXIS2_PLACEMENT_3D ( 'NONE', #4202, #9590, #5648 ) ;
#7788=DIRECTION ( 'NONE',  ( 0.000000000000000000, -6.338944243255235518E-49, 1.000000000000000000 ) ) ;
#7834=DIRECTION ( 'NONE',  ( 0.000000000000000000, -6.338944243255235518E-49, 1.000000000000000000 ) ) ;
#7859=ORIENTED_EDGE ( 'NONE', *, *, #4161, .F. ) ;
#7884=DIRECTION ( 'NONE',  ( 0.000000000000000000, -6.338944243255235518E-49, 1.000000000000000000 ) ) ;
#7899=FACE_OUTER_BOUND ( 'NONE', #6440, .T. ) ;
#7905=EDGE_CURVE ( 'NONE', #4852, #285, #6747, .T. ) ;
#7907=EDGE_CURVE ( 'NONE', #3550, #728, #2487, .T. ) ;
#7914=CARTESIAN_POINT ( 'NONE',  ( -6.919986107680330178, -12.02850919814119557, -1.270000000000007123 ) ) ;
#7919=CARTESIAN_POINT ( 'NONE',  ( -5.986002070941133901, -13.58603705635637304, 0.000000000000000000 ) ) ;
#7921=FACE_BOUND ( 'NONE', #1397, .T. ) ;
#7927=EDGE_CURVE ( 'NONE', #6243, #3552, #10210, .T. ) ;
#7934=EDGE_CURVE ( 'NONE', #8732, #2655, #3632, .T. ) ;
#7950=( GEOMETRIC_REPRESENTATION_CONTEXT ( 3 ) GLOBAL_UNCERTAINTY_ASSIGNED_CONTEXT ( ( #8240 ) ) GLOBAL_UNIT_ASSIGNED_CONTEXT ( ( #3266, #7605, #4293 ) ) REPRESENTATION_CONTEXT ( 'NONE', 'WORKASPACE' ) );
#7969=DIRECTION ( 'NONE',  ( 0.000000000000000000, -6.338944243255235518E-49, 1.000000000000000000 ) ) ;
#7978=CARTESIAN_POINT ( 'NONE',  ( 5.986002070941135678, -13.58603705635637304, -1.270000000000007123 ) ) ;
#7986=VERTEX_POINT ( 'NONE', #6514 ) ;
#8008=ORIENTED_EDGE ( 'NONE', *, *, #2260, .T. ) ;
#8012=CARTESIAN_POINT ( 'NONE',  ( 4.246973736992224246, -14.10948682827615919, -1.270000000000007123 ) ) ;
#8033=CIRCLE ( 'NONE', #1767, 1.816100000000000270 ) ;
#8034=ADVANCED_FACE ( 'NONE', ( #3275 ), #6416, .T. ) ;
#8035=ORIENTED_EDGE ( 'NONE', *, *, #5805, .T. ) ;
#8051=( GEOMETRIC_REPRESENTATION_CONTEXT ( 3 ) GLOBAL_UNCERTAINTY_ASSIGNED_CONTEXT ( ( #4216 ) ) GLOBAL_UNIT_ASSIGNED_CONTEXT ( ( #3524, #6650, #2736 ) ) REPRESENTATION_CONTEXT ( 'NONE', 'WORKASPACE' ) );
#8082=ORIENTED_EDGE ( 'NONE', *, *, #100, .T. ) ;
#8089=SURFACE_STYLE_USAGE ( .BOTH. , #9608 ) ;
#8095=CIRCLE ( 'NONE', #8, 15.44569104238500046 ) ;
#8103=ORIENTED_EDGE ( 'NONE', *, *, #8692, .T. ) ;
#8106=MECHANICAL_DESIGN_GEOMETRIC_PRESENTATION_REPRESENTATION('',(#2332),#5783);
#8137=DIRECTION ( 'NONE',  ( 0.000000000000000000, -6.338944243255235518E-49, 1.000000000000000000 ) ) ;
#8152=CIRCLE ( 'NONE', #10137, 17.72919999999999874 ) ;
#8185=DIRECTION ( 'NONE',  ( 0.000000000000000000, -6.338944243255235518E-49, 1.000000000000000000 ) ) ;
#8195=CARTESIAN_POINT ( 'NONE',  ( 0.000000000000000000, 0.000000000000000000, -1.270000000000007123 ) ) ;
#8209=CARTESIAN_POINT ( 'NONE',  ( -11.48991645990274257, -11.34085470199651979, -1.270000000000007123 ) ) ;
#8233=ORIENTED_EDGE ( 'NONE', *, *, #2812, .T. ) ;
#8240=UNCERTAINTY_MEASURE_WITH_UNIT (LENGTH_MEASURE( 1.000000000000000082E-05 ), #3266, 'distance_accuracy_value', 'NONE');
#8251=ORIENTED_EDGE ( 'NONE', *, *, #3509, .F. ) ;
#8254=AXIS2_PLACEMENT_3D ( 'NONE', #8283, #4410, #1206 ) ;
#8259=EDGE_CURVE ( 'NONE', #7029, #2493, #6748, .T. ) ;
#8264=ORIENTED_EDGE ( 'NONE', *, *, #1932, .F. ) ;
#8283=CARTESIAN_POINT ( 'NONE',  ( 0.000000000000000000, 0.000000000000000000, -1.270000000000007123 ) ) ;
#8311=ADVANCED_FACE ( 'NONE', ( #5033 ), #331, .F. ) ;
#8341=DIRECTION ( 'NONE',  ( 1.000000000000000000, 0.000000000000000000, 0.000000000000000000 ) ) ;
#8346=PRODUCT_DEFINITION_CONTEXT ( 'detailed design', #9444, 'design' ) ;
#8373=LINE ( 'NONE', #3673, #5784 ) ;
#8425=AXIS2_PLACEMENT_3D ( 'NONE', #3798, #4623, #4725 ) ;
#8433=DIRECTION ( 'NONE',  ( 1.000000000000000000, 0.000000000000000000, 0.000000000000000000 ) ) ;
#8443=ORIENTED_EDGE ( 'NONE', *, *, #6843, .F. ) ;
#8470=CIRCLE ( 'NONE', #8811, 15.44569104238500046 ) ;
#8474=ORIENTED_EDGE ( 'NONE', *, *, #6023, .T. ) ;
#8584=CYLINDRICAL_SURFACE ( 'NONE', #19, 1.816100000000000270 ) ;
#8600=ORIENTED_EDGE ( 'NONE', *, *, #8259, .F. ) ;
#8602=VECTOR ( 'NONE', #8137, 1000.000000000000000 ) ;
#8603=DIRECTION ( 'NONE',  ( 1.000000000000000000, 0.000000000000000000, 0.000000000000000000 ) ) ;
#8611=DIRECTION ( 'NONE',  ( 0.000000000000000000, -6.338944243255235518E-49, 1.000000000000000000 ) ) ;
#8613=CARTESIAN_POINT ( 'NONE',  ( 4.995402070941135086, -13.58603705635637304, -1.270000000000007123 ) ) ;
#8636=LINE ( 'NONE', #7756, #5494 ) ;
#8690=EDGE_LOOP ( 'NONE', ( #2063, #4040 ) ) ;
#8692=EDGE_CURVE ( 'NONE', #285, #4852, #8756, .T. ) ;
#8702=ORIENTED_EDGE ( 'NONE', *, *, #3738, .T. ) ;
#8705=CARTESIAN_POINT ( 'NONE',  ( 0.000000000000000000, 0.000000000000000000, -1.270000000000007123 ) ) ;
#8713=VERTEX_POINT ( 'NONE', #7914 ) ;
#8732=VERTEX_POINT ( 'NONE', #4819 ) ;
#8756=CIRCLE ( 'NONE', #7268, 0.9906000000000003691 ) ;
#8773=AXIS2_PLACEMENT_3D ( 'NONE', #1527, #2198, #6309 ) ;
#8811=AXIS2_PLACEMENT_3D ( 'NONE', #276, #954, #7353 ) ;
#8843=DIRECTION ( 'NONE',  ( 1.000000000000000000, 0.000000000000000000, 0.000000000000000000 ) ) ;
#8845=EDGE_CURVE ( 'NONE', #6711, #2258, #10, .T. ) ;
#8859=EDGE_LOOP ( 'NONE', ( #5673, #9986, #6103, #9500 ) ) ;
#8860=DIRECTION ( 'NONE',  ( 0.000000000000000000, -6.338944243255235518E-49, 1.000000000000000000 ) ) ;
#8872=CARTESIAN_POINT ( 'NONE',  ( 5.986002070941135678, -13.58603705635637304, 0.000000000000000000 ) ) ;
#8874=DIRECTION ( 'NONE',  ( 1.000000000000000000, 0.000000000000000000, 0.000000000000000000 ) ) ;
#8895=VERTEX_POINT ( 'NONE', #7472 ) ;
#8916=ORIENTED_EDGE ( 'NONE', *, *, #4549, .F. ) ;
#8921=EDGE_CURVE ( 'NONE', #273, #8732, #5613, .T. ) ;
#8930=DIRECTION ( 'NONE',  ( 0.000000000000000000, 0.000000000000000000, 1.000000000000000000 ) ) ;
#8936=ORIENTED_EDGE ( 'NONE', *, *, #10020, .F. ) ;
#9009=SURFACE_STYLE_USAGE ( .BOTH. , #374 ) ;
#9014=CARTESIAN_POINT ( 'NONE',  ( -5.986002070941133901, -13.58603705635637304, 0.000000000000000000 ) ) ;
#9028=CARTESIAN_POINT ( 'NONE',  ( 4.246973736992224246, -14.10948682827615919, -1.270000000000007123 ) ) ;
#9033=CIRCLE ( 'NONE', #4741, 1.816100000000000270 ) ;
#9076=CARTESIAN_POINT ( 'NONE',  ( 8.787954181158717404, -8.913453481710838844, -1.270000000000007123 ) ) ;
#9085=AXIS2_PLACEMENT_3D ( 'NONE', #6486, #248, #1901 ) ;
#9092=VECTOR ( 'NONE', #7884, 1000.000000000000000 ) ;
#9096=SHAPE_DEFINITION_REPRESENTATION ( #1215, #1047 ) ;
#9100=CIRCLE ( 'NONE', #3154, 3.632200000000000539 ) ;
#9112=SURFACE_STYLE_FILL_AREA ( #9789 ) ;
#9166=ORIENTED_EDGE ( 'NONE', *, *, #3129, .F. ) ;
#9182=CARTESIAN_POINT ( 'NONE',  ( -1.925929944387235853E-31, -1.018491042385001544, -1.270000000000007123 ) ) ;
#9227=DIRECTION ( 'NONE',  ( 0.000000000000000000, 6.338944243255235518E-49, -1.000000000000000000 ) ) ;
#9242=DIRECTION ( 'NONE',  ( 0.000000000000000000, -6.338944243255235518E-49, 1.000000000000000000 ) ) ;
#9252=VERTEX_POINT ( 'NONE', #5175 ) ;
#9255=ORIENTED_EDGE ( 'NONE', *, *, #1061, .F. ) ;
#9265=VECTOR ( 'NONE', #1939, 1000.000000000000000 ) ;
#9267=ORIENTED_EDGE ( 'NONE', *, *, #7221, .F. ) ;
#9285=CARTESIAN_POINT ( 'NONE',  ( 15.44569104238500046, -1.018491042385001544, 0.000000000000000000 ) ) ;
#9298=ORIENTED_EDGE ( 'NONE', *, *, #3626, .F. ) ;
#9318=DIRECTION ( 'NONE',  ( 1.000000000000000000, 0.000000000000000000, 0.000000000000000000 ) ) ;
#9324=DIRECTION ( 'NONE',  ( 0.000000000000000000, -6.338944243255235518E-49, 1.000000000000000000 ) ) ;
#9334=FACE_OUTER_BOUND ( 'NONE', #7375, .T. ) ;
#9358=ORIENTED_EDGE ( 'NONE', *, *, #10144, .F. ) ;
#9373=EDGE_CURVE ( 'NONE', #8713, #2655, #318, .T. ) ;
#9374=LINE ( 'NONE', #2386, #2866 ) ;
#9424=CARTESIAN_POINT ( 'NONE',  ( -5.110041130070070992, -16.97680807127747826, -1.270000000000007123 ) ) ;
#9430=AXIS2_PLACEMENT_3D ( 'NONE', #805, #2502, #4932 ) ;
#9442=CARTESIAN_POINT ( 'NONE',  ( 5.110041130070070992, -16.97680807127747826, 0.000000000000000000 ) ) ;
#9444=APPLICATION_CONTEXT ( 'automotive_design' ) ;
#9447=DIRECTION ( 'NONE',  ( 0.2882273949230682586, -0.9575619921529162637, -1.755378125195845577E-33 ) ) ;
#9456=PRESENTATION_STYLE_ASSIGNMENT (( #8089 ) ) ;
#9496=LINE ( 'NONE', #710, #688 ) ;
#9500=ORIENTED_EDGE ( 'NONE', *, *, #7221, .T. ) ;
#9536=AXIS2_PLACEMENT_3D ( 'NONE', #3410, #9827, #6545 ) ;
#9551=ORIENTED_EDGE ( 'NONE', *, *, #1818, .F. ) ;
#9590=DIRECTION ( 'NONE',  ( 0.000000000000000000, -6.338944243255235518E-49, 1.000000000000000000 ) ) ;
#9599=AXIS2_PLACEMENT_3D ( 'NONE', #8872, #1836, #1786 ) ;
#9601=ADVANCED_FACE ( 'NONE', ( #2331 ), #8584, .T. ) ;
#9608=SURFACE_SIDE_STYLE ('',( #5661 ) ) ;
#9611=EDGE_CURVE ( 'NONE', #5816, #7640, #843, .T. ) ;
#9641=ORIENTED_EDGE ( 'NONE', *, *, #2743, .T. ) ;
#9642=DIRECTION ( 'NONE',  ( 1.000000000000000000, 0.000000000000000000, 0.000000000000000000 ) ) ;
#9689=DIRECTION ( 'NONE',  ( 1.000000000000000000, 0.000000000000000000, 0.000000000000000000 ) ) ;
#9716=ORIENTED_EDGE ( 'NONE', *, *, #7905, .F. ) ;
#9740=DIRECTION ( 'NONE',  ( 0.000000000000000000, -6.338944243255235518E-49, 1.000000000000000000 ) ) ;
#9741=FACE_OUTER_BOUND ( 'NONE', #10034, .T. ) ;
#9758=CIRCLE ( 'NONE', #1670, 1.816100000000000270 ) ;
#9789=FILL_AREA_STYLE ('',( #4399 ) ) ;
#9798=CARTESIAN_POINT ( 'NONE',  ( -1.925929944387235853E-31, -1.018491042385001544, -1.270000000000007123 ) ) ;
#9801=VERTEX_POINT ( 'NONE', #3781 ) ;
#9803=DIRECTION ( 'NONE',  ( 0.000000000000000000, -6.338944243255235518E-49, 1.000000000000000000 ) ) ;
#9827=DIRECTION ( 'NONE',  ( 0.000000000000000000, 6.338944243255235518E-49, -1.000000000000000000 ) ) ;
#9863=ORIENTED_EDGE ( 'NONE', *, *, #6528, .F. ) ;
#9864=AXIS2_PLACEMENT_3D ( 'NONE', #4500, #572, #10026 ) ;
#9868=EDGE_CURVE ( 'NONE', #7540, #1499, #8373, .T. ) ;
#9922=AXIS2_PLACEMENT_3D ( 'NONE', #1816, #218, #162 ) ;
#9942=FACE_OUTER_BOUND ( 'NONE', #127, .T. ) ;
#9954=CARTESIAN_POINT ( 'NONE',  ( -6.976602070941134492, -13.58603705635637304, 0.000000000000000000 ) ) ;
#9975=VECTOR ( 'NONE', #5111, 1000.000000000000000 ) ;
#9976=ORIENTED_EDGE ( 'NONE', *, *, #7905, .T. ) ;
#9977=DIRECTION ( 'NONE',  ( 0.2882273949230689802, 0.9575619921529161527, -1.755378125195851735E-33 ) ) ;
#9979=LINE ( 'NONE', #1962, #9975 ) ;
#9984=DIRECTION ( 'NONE',  ( 0.000000000000000000, -6.338944243255235518E-49, 1.000000000000000000 ) ) ;
#9986=ORIENTED_EDGE ( 'NONE', *, *, #7282, .F. ) ;
#9999=CARTESIAN_POINT ( 'NONE',  ( 0.000000000000000000, 0.000000000000000000, -1.270000000000007123 ) ) ;
#10020=EDGE_CURVE ( 'NONE', #7029, #8895, #4808, .T. ) ;
#10022=AXIS2_PLACEMENT_3D ( 'NONE', #1000, #2641, #850 ) ;
#10026=DIRECTION ( 'NONE',  ( 1.000000000000000000, 0.000000000000000000, 0.000000000000000000 ) ) ;
#10034=EDGE_LOOP ( 'NONE', ( #2946, #5873, #7582, #559 ) ) ;
#10045=EDGE_LOOP ( 'NONE', ( #6015, #8082, #3505, #8702, #1861, #6025, #3399, #1555, #407, #6049, #5728, #2423, #1877 ) ) ;
#10054=CARTESIAN_POINT ( 'NONE',  ( 5.986002070941135678, -13.58603705635637304, 0.000000000000000000 ) ) ;
#10085=AXIS2_PLACEMENT_3D ( 'NONE', #9999, #9803, #5849 ) ;
#10137=AXIS2_PLACEMENT_3D ( 'NONE', #4, #3006, #5334 ) ;
#10144=EDGE_CURVE ( 'NONE', #2655, #2258, #9100, .T. ) ;
#10154=DIRECTION ( 'NONE',  ( 0.000000000000000000, -6.338944243255235518E-49, 1.000000000000000000 ) ) ;
#10158=DIRECTION ( 'NONE',  ( 1.000000000000000000, 0.000000000000000000, 0.000000000000000000 ) ) ;
#10178=CARTESIAN_POINT ( 'NONE',  ( -5.110041130070070992, -16.97680807127747826, 0.000000000000000000 ) ) ;
#10191=DIRECTION ( 'NONE',  ( 1.000000000000000000, 0.000000000000000000, 0.000000000000000000 ) ) ;
#10210=LINE ( 'NONE', #6941, #5940 ) ;
ENDSEC;
END-ISO-10303-21;
